ISO-10303-21;
HEADER;
FILE_DESCRIPTION (('STEP AP203'),
    '1' );
FILE_NAME ('1602p_c_23.step',
    '2026-10-31T14:11:27',
    ( '' ),
    ( '' ),
    'SwSTEP 2.0',
    'SolidWorks 2024',
    '' );
FILE_SCHEMA (( 'AUTOMOTIVE_DESIGN' ));
ENDSEC;

DATA;
#54=VERTEX_POINT ( 'NONE', #10385 ) ;
#80=DIRECTION ( 'NONE',  ( -1.159535895544890222E-14, -2.167612681253619929E-15, -1.000000000000000000 ) ) ;
#174=DIRECTION ( 'NONE',  ( -0.04564792618500997101, -0.9989575901083128651, 2.775557561562890562E-15 ) ) ;
#187=VERTEX_POINT ( 'NONE', #3798 ) ;
#257=DIRECTION ( 'NONE',  ( -1.159535895544890222E-14, -2.167612681253619929E-15, -1.000000000000000000 ) ) ;
#415=DIRECTION ( 'NONE',  ( 1.000000000000000000, 0.000000000000000000, 0.000000000000000000 ) ) ;
#547=VERTEX_POINT ( 'NONE', #14221 ) ;
#615=CYLINDRICAL_SURFACE ( 'NONE', #9091, 2.499999999999999112 ) ;
#634=CYLINDRICAL_SURFACE ( 'NONE', #20520, 5.000000000000001776 ) ;
#786=AXIS2_PLACEMENT_3D ( 'NONE', #9245, #80, #5547 ) ;
#801=EDGE_CURVE ( 'NONE', #547, #8431, #4543, .T. ) ;
#1148=VECTOR ( 'NONE', #3743, 1000.000000000000000 ) ;
#1337=VERTEX_POINT ( 'NONE', #15115 ) ;
#1365=ORIENTED_EDGE ( 'NONE', *, *, #16593, .T. ) ;
#1369=EDGE_CURVE ( 'NONE', #54, #17119, #4676, .T. ) ;
#1728=CARTESIAN_POINT ( 'NONE',  ( -20.00000000397270128, 22.95208919257159863, 5.500000000004459544 ) ) ;
#1733=ADVANCED_FACE ( 'NONE', ( #7738 ), #9165, .T. ) ;
#2003=AXIS2_PLACEMENT_3D ( 'NONE', #8609, #15845, #21425 ) ;
#2058=CARTESIAN_POINT ( 'NONE',  ( -20.00000000397270128, 22.95208919257159863, 5.500000000004459544 ) ) ;
#2194=ORIENTED_EDGE ( 'NONE', *, *, #10217, .F. ) ;
#2285=DIRECTION ( 'NONE',  ( -0.04564792618501069266, -0.9989575901083128651, 2.775557561562892534E-15 ) ) ;
#2446=EDGE_LOOP ( 'NONE', ( #5785, #15604, #21609, #12000 ) ) ;
#2520=CYLINDRICAL_SURFACE ( 'NONE', #6156, 2.499999999999999112 ) ;
#2569=CARTESIAN_POINT ( 'NONE',  ( 0.000000000000000000, 0.000000000000000000, 0.000000000000000000 ) ) ;
#2687=ORIENTED_EDGE ( 'NONE', *, *, #19215, .F. ) ;
#3069=CARTESIAN_POINT ( 'NONE',  ( -19.88588018851017480, 25.44948316784238074, 5.000000000004453327 ) ) ;
#3361=ORIENTED_EDGE ( 'NONE', *, *, #15358, .F. ) ;
#3396=ADVANCED_FACE ( 'NONE', ( #7572, #9122 ), #16356, .T. ) ;
#3399=ORIENTED_EDGE ( 'NONE', *, *, #15358, .T. ) ;
#3557=CIRCLE ( 'NONE', #7365, 5.000000000000001776 ) ;
#3743=DIRECTION ( 'NONE',  ( 1.159535895544890222E-14, 2.167612681253619929E-15, 1.000000000000000000 ) ) ;
#3795=EDGE_LOOP ( 'NONE', ( #1365, #13169 ) ) ;
#3798=CARTESIAN_POINT ( 'NONE',  ( -20.22823963489775068, 17.95730124203003442, 5.000000000004473755 ) ) ;
#3829=DIRECTION ( 'NONE',  ( 1.159535895544890222E-14, 2.167612681253619929E-15, 1.000000000000000000 ) ) ;
#3830=FACE_BOUND ( 'NONE', #19166, .T. ) ;
#3903=CIRCLE ( 'NONE', #13410, 2.499999999999999112 ) ;
#3960=FACE_OUTER_BOUND ( 'NONE', #21181, .T. ) ;
#4017=( GEOMETRIC_REPRESENTATION_CONTEXT ( 3 ) GLOBAL_UNCERTAINTY_ASSIGNED_CONTEXT ( ( #19409 ) ) GLOBAL_UNIT_ASSIGNED_CONTEXT ( ( #12292, #19623, #15829 ) ) REPRESENTATION_CONTEXT ( 'NONE', 'WORKASPACE' ) );
#4118=DIRECTION ( 'NONE',  ( -0.04564792618501069266, -0.9989575901083128651, 2.775557561562892534E-15 ) ) ;
#4543=CIRCLE ( 'NONE', #20848, 5.000000000000001776 ) ;
#4676=LINE ( 'NONE', #12052, #14681 ) ;
#4776=ORIENTED_EDGE ( 'NONE', *, *, #801, .T. ) ;
#4836=VERTEX_POINT ( 'NONE', #14260 ) ;
#5330=EDGE_CURVE ( 'NONE', #1337, #547, #21909, .T. ) ;
#5547=DIRECTION ( 'NONE',  ( -1.000000000000000000, 0.000000000000000000, 1.159535895544890222E-14 ) ) ;
#5688=DIRECTION ( 'NONE',  ( -1.159535895544890222E-14, -2.167612681253619929E-15, -1.000000000000000000 ) ) ;
#5730=VERTEX_POINT ( 'NONE', #8375 ) ;
#5785=ORIENTED_EDGE ( 'NONE', *, *, #5330, .F. ) ;
#5835=EDGE_LOOP ( 'NONE', ( #10907, #15078, #4776, #18429 ) ) ;
#5992=ADVANCED_FACE ( 'NONE', ( #3830, #3960 ), #21774, .F. ) ;
#6056=ADVANCED_FACE ( 'NONE', ( #22580 ), #615, .F. ) ;
#6156=AXIS2_PLACEMENT_3D ( 'NONE', #18568, #20225, #13219 ) ;
#6353=VECTOR ( 'NONE', #16152, 1000.000000000000000 ) ;
#6403=CLOSED_SHELL ( 'NONE', ( #10600, #6056, #16190, #1733, #5992, #3396 ) ) ;
#6462=ORIENTED_EDGE ( 'NONE', *, *, #801, .F. ) ;
#6490=CARTESIAN_POINT ( 'NONE',  ( -20.00000000397270128, 22.95208919257159863, 5.000000000004460432 ) ) ;
#7178=CARTESIAN_POINT ( 'NONE',  ( -20.00000000397270128, 22.95208919257159863, 5.000000000004460432 ) ) ;
#7344=CARTESIAN_POINT ( 'NONE',  ( -20.22823963489775068, 17.95730124203003442, 5.500000000004473755 ) ) ;
#7365=AXIS2_PLACEMENT_3D ( 'NONE', #11748, #20860, #18868 ) ;
#7572=FACE_BOUND ( 'NONE', #15168, .T. ) ;
#7683=ORIENTED_EDGE ( 'NONE', *, *, #10217, .T. ) ;
#7702=ORIENTED_EDGE ( 'NONE', *, *, #20211, .F. ) ;
#7738=FACE_OUTER_BOUND ( 'NONE', #2446, .T. ) ;
#7894=DIRECTION ( 'NONE',  ( 1.159535895544890222E-14, 2.167612681253619929E-15, 1.000000000000000000 ) ) ;
#8325=PRODUCT ( '1602p_c_23', '1602p_c_23', '', ( #15290 ) ) ;
#8375=CARTESIAN_POINT ( 'NONE',  ( -19.88588018851017125, 25.44948316784238074, 5.500000000004452438 ) ) ;
#8405=ORIENTED_EDGE ( 'NONE', *, *, #1369, .F. ) ;
#8431=VERTEX_POINT ( 'NONE', #7344 ) ;
#8609=CARTESIAN_POINT ( 'NONE',  ( -20.00000000397270128, 22.95208919257159863, 5.500000000004459544 ) ) ;
#8656=EDGE_CURVE ( 'NONE', #17119, #5730, #12302, .T. ) ;
#8680=APPLICATION_CONTEXT ( 'configuration controlled 3d designs of mechanical parts and assemblies' ) ;
#8960=DIRECTION ( 'NONE',  ( -1.000000000000000000, 0.000000000000000000, 1.159535895544890222E-14 ) ) ;
#8992=DIRECTION ( 'NONE',  ( -1.159535895544890222E-14, -2.167612681253619929E-15, -1.000000000000000000 ) ) ;
#9091=AXIS2_PLACEMENT_3D ( 'NONE', #10038, #17264, #2285 ) ;
#9122=FACE_OUTER_BOUND ( 'NONE', #3795, .T. ) ;
#9165=CYLINDRICAL_SURFACE ( 'NONE', #9894, 5.000000000000001776 ) ;
#9225=CARTESIAN_POINT ( 'NONE',  ( -20.00000000397270128, 22.95208919257159863, 5.500000000004459544 ) ) ;
#9245=CARTESIAN_POINT ( 'NONE',  ( -20.00000000397270128, 22.95208919257159863, 5.000000000004460432 ) ) ;
#9560=VECTOR ( 'NONE', #22772, 1000.000000000000000 ) ;
#9635=AXIS2_PLACEMENT_3D ( 'NONE', #20732, #18617, #16826 ) ;
#9697=CARTESIAN_POINT ( 'NONE',  ( -20.00000000397270128, 22.95208919257159863, 5.000000000004460432 ) ) ;
#9807=DIRECTION ( 'NONE',  ( -0.04564792618500997101, -0.9989575901083128651, 2.775557561562890562E-15 ) ) ;
#9810=ORIENTED_EDGE ( 'NONE', *, *, #19215, .T. ) ;
#9894=AXIS2_PLACEMENT_3D ( 'NONE', #11212, #14853, #16402 ) ;
#10003=AXIS2_PLACEMENT_3D ( 'NONE', #18656, #5688, #20659 ) ;
#10038=CARTESIAN_POINT ( 'NONE',  ( -20.00000000397270128, 22.95208919257159863, 5.000000000004460432 ) ) ;
#10043=DIRECTION ( 'NONE',  ( 1.159535895544890222E-14, 2.167612681253619929E-15, 1.000000000000000000 ) ) ;
#10217=EDGE_CURVE ( 'NONE', #54, #4836, #14823, .T. ) ;
#10375=SHAPE_REPRESENTATION ( '1602p_c_23', ( #12739 ), #4017 ) ;
#10385=CARTESIAN_POINT ( 'NONE',  ( -20.11411981943522775, 20.45469521730081652, 5.000000000004466649 ) ) ;
#10600=ADVANCED_FACE ( 'NONE', ( #16800 ), #634, .T. ) ;
#10721=LINE ( 'NONE', #16267, #6353 ) ;
#10725=EDGE_LOOP ( 'NONE', ( #3361, #2194, #12155, #19449 ) ) ;
#10731=ORIENTED_EDGE ( 'NONE', *, *, #8656, .F. ) ;
#10766=CIRCLE ( 'NONE', #10003, 5.000000000000001776 ) ;
#10907=ORIENTED_EDGE ( 'NONE', *, *, #18253, .F. ) ;
#11212=CARTESIAN_POINT ( 'NONE',  ( -20.00000000397270128, 22.95208919257159863, 5.000000000004460432 ) ) ;
#11340=FACE_OUTER_BOUND ( 'NONE', #10725, .T. ) ;
#11567=EDGE_CURVE ( 'NONE', #187, #8431, #10721, .T. ) ;
#11748=CARTESIAN_POINT ( 'NONE',  ( -20.00000000397270128, 22.95208919257159863, 5.000000000004460432 ) ) ;
#11760=AXIS2_PLACEMENT_3D ( 'NONE', #2058, #257, #8960 ) ;
#12000=ORIENTED_EDGE ( 'NONE', *, *, #20211, .T. ) ;
#12052=CARTESIAN_POINT ( 'NONE',  ( -20.11411981943522775, 20.45469521730081652, 5.000000000004466649 ) ) ;
#12155=ORIENTED_EDGE ( 'NONE', *, *, #1369, .T. ) ;
#12292=( LENGTH_UNIT ( ) NAMED_UNIT ( * ) SI_UNIT ( .MILLI., .METRE. ) );
#12302=CIRCLE ( 'NONE', #9635, 2.499999999999999112 ) ;
#12650=DIRECTION ( 'NONE',  ( -0.04564792618501069266, -0.9989575901083128651, 2.775557561562892534E-15 ) ) ;
#12739=AXIS2_PLACEMENT_3D ( 'NONE', #2569, #13380, #415 ) ;
#12998=CIRCLE ( 'NONE', #13763, 5.000000000000001776 ) ;
#13169=ORIENTED_EDGE ( 'NONE', *, *, #18253, .T. ) ;
#13219=DIRECTION ( 'NONE',  ( -0.04564792618501069266, -0.9989575901083128651, 2.775557561562892534E-15 ) ) ;
#13380=DIRECTION ( 'NONE',  ( 0.000000000000000000, 0.000000000000000000, 1.000000000000000000 ) ) ;
#13410=AXIS2_PLACEMENT_3D ( 'NONE', #7178, #3829, #12650 ) ;
#13763=AXIS2_PLACEMENT_3D ( 'NONE', #1728, #8992, #20374 ) ;
#14221=CARTESIAN_POINT ( 'NONE',  ( -19.77176037304764833, 27.94687714311316284, 5.500000000004446221 ) ) ;
#14260=CARTESIAN_POINT ( 'NONE',  ( -19.88588018851017125, 25.44948316784238074, 5.000000000004453327 ) ) ;
#14560=CARTESIAN_POINT ( 'NONE',  ( -20.11411981943522775, 20.45469521730081652, 5.500000000004466649 ) ) ;
#14565=CARTESIAN_POINT ( 'NONE',  ( -19.77176037304765188, 27.94687714311316640, 5.000000000004446221 ) ) ;
#14681=VECTOR ( 'NONE', #10043, 1000.000000000000000 ) ;
#14823=CIRCLE ( 'NONE', #22764, 2.499999999999999112 ) ;
#14853=DIRECTION ( 'NONE',  ( 1.159535895544890222E-14, 2.167612681253619929E-15, 1.000000000000000000 ) ) ;
#15078=ORIENTED_EDGE ( 'NONE', *, *, #5330, .T. ) ;
#15115=CARTESIAN_POINT ( 'NONE',  ( -19.77176037304764833, 27.94687714311316284, 5.000000000004446221 ) ) ;
#15168=EDGE_LOOP ( 'NONE', ( #7683, #9810 ) ) ;
#15290=MECHANICAL_CONTEXT ( 'NONE', #8680, 'mechanical' ) ;
#15358=EDGE_CURVE ( 'NONE', #4836, #5730, #15536, .T. ) ;
#15536=LINE ( 'NONE', #3069, #9560 ) ;
#15604=ORIENTED_EDGE ( 'NONE', *, *, #16593, .F. ) ;
#15829=( NAMED_UNIT ( * ) SI_UNIT ( $, .STERADIAN. ) SOLID_ANGLE_UNIT ( ) );
#15845=DIRECTION ( 'NONE',  ( -1.159535895544890222E-14, -2.167612681253619929E-15, -1.000000000000000000 ) ) ;
#15896=ORIENTED_EDGE ( 'NONE', *, *, #8656, .T. ) ;
#16152=DIRECTION ( 'NONE',  ( 1.159535895544890222E-14, 2.167612681253619929E-15, 1.000000000000000000 ) ) ;
#16172=SHAPE_REPRESENTATION_RELATIONSHIP ( 'NONE' , 'NONE' ,  #10375, #16174 ) ;
#16174=ADVANCED_BREP_SHAPE_REPRESENTATION ( '', ( #17306, #12739 ), #4017 ) ;
#16190=ADVANCED_FACE ( 'NONE', ( #11340 ), #2520, .F. ) ;
#16267=CARTESIAN_POINT ( 'NONE',  ( -20.22823963489775068, 17.95730124203003442, 5.000000000004473755 ) ) ;
#16356=PLANE ( 'NONE',  #786 ) ;
#16402=DIRECTION ( 'NONE',  ( -0.04564792618500997101, -0.9989575901083128651, 2.775557561562890562E-15 ) ) ;
#16455=DIRECTION ( 'NONE',  ( -1.159535895544890222E-14, -2.167612681253619929E-15, -1.000000000000000000 ) ) ;
#16593=EDGE_CURVE ( 'NONE', #187, #1337, #10766, .T. ) ;
#16800=FACE_OUTER_BOUND ( 'NONE', #5835, .T. ) ;
#16826=DIRECTION ( 'NONE',  ( -0.04564792618501069266, -0.9989575901083128651, 2.775557561562892534E-15 ) ) ;
#17119=VERTEX_POINT ( 'NONE', #14560 ) ;
#17264=DIRECTION ( 'NONE',  ( 1.159535895544890222E-14, 2.167612681253619929E-15, 1.000000000000000000 ) ) ;
#17306=MANIFOLD_SOLID_BREP ( 'Imported1', #6403 ) ;
#17820=PRODUCT_DEFINITION_SHAPE ( 'NONE', 'NONE',  #19247 ) ;
#17865=EDGE_LOOP ( 'NONE', ( #2687, #3399, #10731, #8405 ) ) ;
#18253=EDGE_CURVE ( 'NONE', #1337, #187, #3557, .T. ) ;
#18429=ORIENTED_EDGE ( 'NONE', *, *, #11567, .F. ) ;
#18568=CARTESIAN_POINT ( 'NONE',  ( -20.00000000397270128, 22.95208919257159863, 5.000000000004460432 ) ) ;
#18617=DIRECTION ( 'NONE',  ( -1.159535895544890222E-14, -2.167612681253619929E-15, -1.000000000000000000 ) ) ;
#18621=DIRECTION ( 'NONE',  ( 1.159535895544890222E-14, 2.167612681253619929E-15, 1.000000000000000000 ) ) ;
#18656=CARTESIAN_POINT ( 'NONE',  ( -20.00000000397270128, 22.95208919257159863, 5.000000000004460432 ) ) ;
#18868=DIRECTION ( 'NONE',  ( -0.04564792618500997101, -0.9989575901083128651, 2.775557561562890562E-15 ) ) ;
#19072=EDGE_CURVE ( 'NONE', #5730, #17119, #22461, .T. ) ;
#19166=EDGE_LOOP ( 'NONE', ( #15896, #19375 ) ) ;
#19215=EDGE_CURVE ( 'NONE', #4836, #54, #3903, .T. ) ;
#19247=PRODUCT_DEFINITION ( 'UNKNOWN', '', #19768, #21088 ) ;
#19375=ORIENTED_EDGE ( 'NONE', *, *, #19072, .T. ) ;
#19409=UNCERTAINTY_MEASURE_WITH_UNIT (LENGTH_MEASURE( 1.000000000000000082E-05 ), #12292, 'distance_accuracy_value', 'NONE');
#19449=ORIENTED_EDGE ( 'NONE', *, *, #19072, .F. ) ;
#19623=( NAMED_UNIT ( * ) PLANE_ANGLE_UNIT ( ) SI_UNIT ( $, .RADIAN. ) );
#19768=PRODUCT_DEFINITION_FORMATION_WITH_SPECIFIED_SOURCE ( 'ANY', '', #8325, .NOT_KNOWN. ) ;
#20211=EDGE_CURVE ( 'NONE', #8431, #547, #12998, .T. ) ;
#20225=DIRECTION ( 'NONE',  ( 1.159535895544890222E-14, 2.167612681253619929E-15, 1.000000000000000000 ) ) ;
#20374=DIRECTION ( 'NONE',  ( -0.04564792618500997101, -0.9989575901083128651, 2.775557561562890562E-15 ) ) ;
#20520=AXIS2_PLACEMENT_3D ( 'NONE', #9697, #7894, #9807 ) ;
#20535=APPLICATION_CONTEXT ( 'configuration controlled 3d designs of mechanical parts and assemblies' ) ;
#20659=DIRECTION ( 'NONE',  ( -0.04564792618500997101, -0.9989575901083128651, 2.775557561562890562E-15 ) ) ;
#20732=CARTESIAN_POINT ( 'NONE',  ( -20.00000000397270128, 22.95208919257159863, 5.500000000004459544 ) ) ;
#20848=AXIS2_PLACEMENT_3D ( 'NONE', #9225, #16455, #174 ) ;
#20860=DIRECTION ( 'NONE',  ( -1.159535895544890222E-14, -2.167612681253619929E-15, -1.000000000000000000 ) ) ;
#21088=DESIGN_CONTEXT ( 'detailed design', #20535, 'design' ) ;
#21181=EDGE_LOOP ( 'NONE', ( #7702, #6462 ) ) ;
#21425=DIRECTION ( 'NONE',  ( -0.04564792618501069266, -0.9989575901083128651, 2.775557561562892534E-15 ) ) ;
#21609=ORIENTED_EDGE ( 'NONE', *, *, #11567, .T. ) ;
#21774=PLANE ( 'NONE',  #11760 ) ;
#21909=LINE ( 'NONE', #14565, #1148 ) ;
#22461=CIRCLE ( 'NONE', #2003, 2.499999999999999112 ) ;
#22580=FACE_OUTER_BOUND ( 'NONE', #17865, .T. ) ;
#22635=SHAPE_DEFINITION_REPRESENTATION ( #17820, #10375 ) ;
#22764=AXIS2_PLACEMENT_3D ( 'NONE', #6490, #18621, #4118 ) ;
#22772=DIRECTION ( 'NONE',  ( 1.159535895544890222E-14, 2.167612681253619929E-15, 1.000000000000000000 ) ) ;
#23529=COLOUR_RGB('Sky Blue', 0.31764706, 0.68627451, 0.89019608);
#23530=FILL_AREA_STYLE_COLOUR('',#23529);
#23531=FILL_AREA_STYLE('',(#23530));
#23532=SURFACE_STYLE_FILL_AREA(#23531);
#23533=SURFACE_SIDE_STYLE('',(#23532));
#23534=SURFACE_STYLE_USAGE(.BOTH.,#23533);
#23535=PRESENTATION_STYLE_ASSIGNMENT((#23534));
#23607=STYLED_ITEM('',(#23535),#17306);
#23608=MECHANICAL_DESIGN_GEOMETRIC_PRESENTATION_REPRESENTATION('',(#23607),#4017);
ENDSEC;
END-ISO-10303-21;
